ISO-10303-21;
HEADER;
/* Generated by software containing ST-Developer
 * from STEP Tools, Inc. (www.steptools.com) 
 */

FILE_DESCRIPTION(
/* description */ ('STEP AP214'),
/* implementation_level */ '2;1');

FILE_NAME(
/* name */ 'Socket Head Cap Screw M6x25.step',
/* time_stamp */ '2026-11-15T14:55:55-08:00',
/* author */ (''),
/* organization */ (''),
/* preprocessor_version */ 'ST-DEVELOPER v20.2',
/* originating_system */ 'Autodesk Translation Framework v15.17.0.0',
/* authorisation */ '');

FILE_SCHEMA (('AUTOMOTIVE_DESIGN { 1 0 10303 214 3 1 1 }'));
ENDSEC;

DATA;
#10=MECHANICAL_DESIGN_GEOMETRIC_PRESENTATION_REPRESENTATION('',(#957),#57079);
#893=SHAPE_REPRESENTATION_RELATIONSHIP('SRR','None',#57283,#922);
#922=ADVANCED_BREP_SHAPE_REPRESENTATION('',(#994),#57075);
#957=STYLED_ITEM('',(#57444),#994);
#994=MANIFOLD_SOLID_BREP('Body1',#24557);
#1331=FACE_BOUND('',#5173,.T.);
#1332=FACE_BOUND('',#5175,.T.);
#2053=PLANE('',#27305);
#2054=PLANE('',#27306);
#2055=PLANE('',#27307);
#2056=PLANE('',#27308);
#2057=PLANE('',#27309);
#2058=PLANE('',#27310);
#2059=PLANE('',#27311);
#2060=PLANE('',#27312);
#2061=PLANE('',#27313);
#2062=PLANE('',#27314);
#2151=CONICAL_SURFACE('',#27297,5.,0.785398163397451);
#2152=CONICAL_SURFACE('',#27299,2.4585,0.785398163397442);
#3461=FACE_OUTER_BOUND('',#5167,.T.);
#3462=FACE_OUTER_BOUND('',#5168,.T.);
#3463=FACE_OUTER_BOUND('',#5169,.T.);
#3464=FACE_OUTER_BOUND('',#5170,.T.);
#3465=FACE_OUTER_BOUND('',#5171,.T.);
#3466=FACE_OUTER_BOUND('',#5172,.T.);
#3467=FACE_OUTER_BOUND('',#5174,.T.);
#3468=FACE_OUTER_BOUND('',#5176,.T.);
#3469=FACE_OUTER_BOUND('',#5177,.T.);
#3470=FACE_OUTER_BOUND('',#5178,.T.);
#3471=FACE_OUTER_BOUND('',#5179,.T.);
#3472=FACE_OUTER_BOUND('',#5180,.T.);
#3473=FACE_OUTER_BOUND('',#5181,.T.);
#3474=FACE_OUTER_BOUND('',#5182,.T.);
#5167=EDGE_LOOP('',(#22444,#22445,#22446,#22447));
#5168=EDGE_LOOP('',(#22448,#22449,#22450,#22451));
#5169=EDGE_LOOP('',(#22452,#22453,#22454,#22455,#22456));
#5170=EDGE_LOOP('',(#22457,#22458,#22459,#22460,#22461));
#5171=EDGE_LOOP('',(#22462));
#5172=EDGE_LOOP('',(#22463));
#5173=EDGE_LOOP('',(#22464,#22465,#22466,#22467,#22468,#22469));
#5174=EDGE_LOOP('',(#22470));
#5175=EDGE_LOOP('',(#22471));
#5176=EDGE_LOOP('',(#22472,#22473,#22474,#22475));
#5177=EDGE_LOOP('',(#22476,#22477,#22478,#22479));
#5178=EDGE_LOOP('',(#22480,#22481,#22482,#22483));
#5179=EDGE_LOOP('',(#22484,#22485,#22486,#22487));
#5180=EDGE_LOOP('',(#22488,#22489,#22490,#22491));
#5181=EDGE_LOOP('',(#22492,#22493,#22494,#22495));
#5182=EDGE_LOOP('',(#22496,#22497,#22498,#22499,#22500,#22501));
#7113=LINE('',#56621,#9080);
#7114=LINE('',#56625,#9081);
#7115=LINE('',#56632,#9082);
#7116=LINE('',#56637,#9083);
#7117=LINE('',#56643,#9084);
#7118=LINE('',#56645,#9085);
#7119=LINE('',#56647,#9086);
#7120=LINE('',#56649,#9087);
#7121=LINE('',#56651,#9088);
#7122=LINE('',#56652,#9089);
#7123=LINE('',#56656,#9090);
#7124=LINE('',#56658,#9091);
#7125=LINE('',#56659,#9092);
#7126=LINE('',#56662,#9093);
#7127=LINE('',#56663,#9094);
#7128=LINE('',#56666,#9095);
#7129=LINE('',#56667,#9096);
#7130=LINE('',#56670,#9097);
#7131=LINE('',#56671,#9098);
#7132=LINE('',#56674,#9099);
#7133=LINE('',#56675,#9100);
#7134=LINE('',#56677,#9101);
#9080=VECTOR('',#34165,5.);
#9081=VECTOR('',#34170,5.);
#9082=VECTOR('',#34177,2.4585);
#9083=VECTOR('',#34184,3.);
#9084=VECTOR('',#34191,1000.);
#9085=VECTOR('',#34192,1000.);
#9086=VECTOR('',#34193,1000.);
#9087=VECTOR('',#34194,1000.);
#9088=VECTOR('',#34195,1000.);
#9089=VECTOR('',#34196,1000.);
#9090=VECTOR('',#34201,1000.);
#9091=VECTOR('',#34202,1000.);
#9092=VECTOR('',#34203,1000.);
#9093=VECTOR('',#34206,1000.);
#9094=VECTOR('',#34207,1000.);
#9095=VECTOR('',#34210,1000.);
#9096=VECTOR('',#34211,1000.);
#9097=VECTOR('',#34214,1000.);
#9098=VECTOR('',#34215,1000.);
#9099=VECTOR('',#34218,1000.);
#9100=VECTOR('',#34219,1000.);
#9101=VECTOR('',#34222,1000.);
#10235=CIRCLE('',#27295,5.);
#10236=CIRCLE('',#27296,5.);
#10237=CIRCLE('',#27298,4.4);
#10238=CIRCLE('',#27300,3.);
#10239=CIRCLE('',#27301,2.4585);
#10240=CIRCLE('',#27302,3.);
#10241=CIRCLE('',#27304,3.);
#12406=VERTEX_POINT('',#56618);
#12407=VERTEX_POINT('',#56620);
#12408=VERTEX_POINT('',#56624);
#12409=VERTEX_POINT('',#56628);
#12410=VERTEX_POINT('',#56629);
#12411=VERTEX_POINT('',#56631);
#12412=VERTEX_POINT('',#56636);
#12413=VERTEX_POINT('',#56641);
#12414=VERTEX_POINT('',#56642);
#12415=VERTEX_POINT('',#56644);
#12416=VERTEX_POINT('',#56646);
#12417=VERTEX_POINT('',#56648);
#12418=VERTEX_POINT('',#56650);
#12419=VERTEX_POINT('',#56655);
#12420=VERTEX_POINT('',#56657);
#12421=VERTEX_POINT('',#56661);
#12422=VERTEX_POINT('',#56665);
#12423=VERTEX_POINT('',#56669);
#12424=VERTEX_POINT('',#56673);
#15767=EDGE_CURVE('',#12406,#12406,#10235,.T.);
#15768=EDGE_CURVE('',#12406,#12407,#7113,.T.);
#15769=EDGE_CURVE('',#12407,#12407,#10236,.T.);
#15770=EDGE_CURVE('',#12407,#12408,#7114,.T.);
#15771=EDGE_CURVE('',#12408,#12408,#10237,.T.);
#15772=EDGE_CURVE('',#12409,#12410,#10238,.T.);
#15773=EDGE_CURVE('',#12410,#12411,#7115,.T.);
#15774=EDGE_CURVE('',#12411,#12411,#10239,.T.);
#15775=EDGE_CURVE('',#12410,#12409,#10240,.T.);
#15776=EDGE_CURVE('',#12409,#12412,#7116,.T.);
#15777=EDGE_CURVE('',#12412,#12412,#10241,.T.);
#15778=EDGE_CURVE('',#12413,#12414,#7117,.T.);
#15779=EDGE_CURVE('',#12415,#12413,#7118,.T.);
#15780=EDGE_CURVE('',#12416,#12415,#7119,.T.);
#15781=EDGE_CURVE('',#12417,#12416,#7120,.T.);
#15782=EDGE_CURVE('',#12418,#12417,#7121,.T.);
#15783=EDGE_CURVE('',#12414,#12418,#7122,.T.);
#15784=EDGE_CURVE('',#12419,#12414,#7123,.T.);
#15785=EDGE_CURVE('',#12420,#12419,#7124,.T.);
#15786=EDGE_CURVE('',#12420,#12413,#7125,.T.);
#15787=EDGE_CURVE('',#12421,#12420,#7126,.T.);
#15788=EDGE_CURVE('',#12421,#12415,#7127,.T.);
#15789=EDGE_CURVE('',#12422,#12421,#7128,.T.);
#15790=EDGE_CURVE('',#12422,#12416,#7129,.T.);
#15791=EDGE_CURVE('',#12423,#12422,#7130,.T.);
#15792=EDGE_CURVE('',#12423,#12417,#7131,.T.);
#15793=EDGE_CURVE('',#12424,#12423,#7132,.T.);
#15794=EDGE_CURVE('',#12424,#12418,#7133,.T.);
#15795=EDGE_CURVE('',#12419,#12424,#7134,.T.);
#22444=ORIENTED_EDGE('',*,*,#15767,.F.);
#22445=ORIENTED_EDGE('',*,*,#15768,.T.);
#22446=ORIENTED_EDGE('',*,*,#15769,.T.);
#22447=ORIENTED_EDGE('',*,*,#15768,.F.);
#22448=ORIENTED_EDGE('',*,*,#15769,.F.);
#22449=ORIENTED_EDGE('',*,*,#15770,.T.);
#22450=ORIENTED_EDGE('',*,*,#15771,.T.);
#22451=ORIENTED_EDGE('',*,*,#15770,.F.);
#22452=ORIENTED_EDGE('',*,*,#15772,.T.);
#22453=ORIENTED_EDGE('',*,*,#15773,.T.);
#22454=ORIENTED_EDGE('',*,*,#15774,.F.);
#22455=ORIENTED_EDGE('',*,*,#15773,.F.);
#22456=ORIENTED_EDGE('',*,*,#15775,.T.);
#22457=ORIENTED_EDGE('',*,*,#15772,.F.);
#22458=ORIENTED_EDGE('',*,*,#15776,.T.);
#22459=ORIENTED_EDGE('',*,*,#15777,.T.);
#22460=ORIENTED_EDGE('',*,*,#15776,.F.);
#22461=ORIENTED_EDGE('',*,*,#15775,.F.);
#22462=ORIENTED_EDGE('',*,*,#15774,.T.);
#22463=ORIENTED_EDGE('',*,*,#15771,.F.);
#22464=ORIENTED_EDGE('',*,*,#15778,.F.);
#22465=ORIENTED_EDGE('',*,*,#15779,.F.);
#22466=ORIENTED_EDGE('',*,*,#15780,.F.);
#22467=ORIENTED_EDGE('',*,*,#15781,.F.);
#22468=ORIENTED_EDGE('',*,*,#15782,.F.);
#22469=ORIENTED_EDGE('',*,*,#15783,.F.);
#22470=ORIENTED_EDGE('',*,*,#15767,.T.);
#22471=ORIENTED_EDGE('',*,*,#15777,.F.);
#22472=ORIENTED_EDGE('',*,*,#15778,.T.);
#22473=ORIENTED_EDGE('',*,*,#15784,.F.);
#22474=ORIENTED_EDGE('',*,*,#15785,.F.);
#22475=ORIENTED_EDGE('',*,*,#15786,.T.);
#22476=ORIENTED_EDGE('',*,*,#15779,.T.);
#22477=ORIENTED_EDGE('',*,*,#15786,.F.);
#22478=ORIENTED_EDGE('',*,*,#15787,.F.);
#22479=ORIENTED_EDGE('',*,*,#15788,.T.);
#22480=ORIENTED_EDGE('',*,*,#15780,.T.);
#22481=ORIENTED_EDGE('',*,*,#15788,.F.);
#22482=ORIENTED_EDGE('',*,*,#15789,.F.);
#22483=ORIENTED_EDGE('',*,*,#15790,.T.);
#22484=ORIENTED_EDGE('',*,*,#15781,.T.);
#22485=ORIENTED_EDGE('',*,*,#15790,.F.);
#22486=ORIENTED_EDGE('',*,*,#15791,.F.);
#22487=ORIENTED_EDGE('',*,*,#15792,.T.);
#22488=ORIENTED_EDGE('',*,*,#15782,.T.);
#22489=ORIENTED_EDGE('',*,*,#15792,.F.);
#22490=ORIENTED_EDGE('',*,*,#15793,.F.);
#22491=ORIENTED_EDGE('',*,*,#15794,.T.);
#22492=ORIENTED_EDGE('',*,*,#15783,.T.);
#22493=ORIENTED_EDGE('',*,*,#15794,.F.);
#22494=ORIENTED_EDGE('',*,*,#15795,.F.);
#22495=ORIENTED_EDGE('',*,*,#15784,.T.);
#22496=ORIENTED_EDGE('',*,*,#15785,.T.);
#22497=ORIENTED_EDGE('',*,*,#15795,.T.);
#22498=ORIENTED_EDGE('',*,*,#15793,.T.);
#22499=ORIENTED_EDGE('',*,*,#15791,.T.);
#22500=ORIENTED_EDGE('',*,*,#15789,.T.);
#22501=ORIENTED_EDGE('',*,*,#15787,.T.);
#23138=CYLINDRICAL_SURFACE('',#27294,5.);
#23139=CYLINDRICAL_SURFACE('',#27303,3.);
#24453=ADVANCED_FACE('',(#3461),#23138,.T.);
#24454=ADVANCED_FACE('',(#3462),#2151,.T.);
#24455=ADVANCED_FACE('',(#3463),#2152,.T.);
#24456=ADVANCED_FACE('',(#3464),#23139,.T.);
#24457=ADVANCED_FACE('',(#3465),#2053,.T.);
#24458=ADVANCED_FACE('',(#3466,#1331),#2054,.T.);
#24459=ADVANCED_FACE('',(#3467,#1332),#2055,.T.);
#24460=ADVANCED_FACE('',(#3468),#2056,.F.);
#24461=ADVANCED_FACE('',(#3469),#2057,.F.);
#24462=ADVANCED_FACE('',(#3470),#2058,.F.);
#24463=ADVANCED_FACE('',(#3471),#2059,.F.);
#24464=ADVANCED_FACE('',(#3472),#2060,.F.);
#24465=ADVANCED_FACE('',(#3473),#2061,.F.);
#24466=ADVANCED_FACE('',(#3474),#2062,.T.);
#24557=CLOSED_SHELL('',(#24453,#24454,#24455,#24456,#24457,#24458,#24459,
#24460,#24461,#24462,#24463,#24464,#24465,#24466));
#27293=AXIS2_PLACEMENT_3D('',#56616,#34159,#34160);
#27294=AXIS2_PLACEMENT_3D('',#56617,#34161,#34162);
#27295=AXIS2_PLACEMENT_3D('',#56619,#34163,#34164);
#27296=AXIS2_PLACEMENT_3D('',#56622,#34166,#34167);
#27297=AXIS2_PLACEMENT_3D('',#56623,#34168,#34169);
#27298=AXIS2_PLACEMENT_3D('',#56626,#34171,#34172);
#27299=AXIS2_PLACEMENT_3D('',#56627,#34173,#34174);
#27300=AXIS2_PLACEMENT_3D('',#56630,#34175,#34176);
#27301=AXIS2_PLACEMENT_3D('',#56633,#34178,#34179);
#27302=AXIS2_PLACEMENT_3D('',#56634,#34180,#34181);
#27303=AXIS2_PLACEMENT_3D('',#56635,#34182,#34183);
#27304=AXIS2_PLACEMENT_3D('',#56638,#34185,#34186);
#27305=AXIS2_PLACEMENT_3D('',#56639,#34187,#34188);
#27306=AXIS2_PLACEMENT_3D('',#56640,#34189,#34190);
#27307=AXIS2_PLACEMENT_3D('',#56653,#34197,#34198);
#27308=AXIS2_PLACEMENT_3D('',#56654,#34199,#34200);
#27309=AXIS2_PLACEMENT_3D('',#56660,#34204,#34205);
#27310=AXIS2_PLACEMENT_3D('',#56664,#34208,#34209);
#27311=AXIS2_PLACEMENT_3D('',#56668,#34212,#34213);
#27312=AXIS2_PLACEMENT_3D('',#56672,#34216,#34217);
#27313=AXIS2_PLACEMENT_3D('',#56676,#34220,#34221);
#27314=AXIS2_PLACEMENT_3D('',#56678,#34223,#34224);
#34159=DIRECTION('axis',(0.,0.,1.));
#34160=DIRECTION('refdir',(1.,0.,0.));
#34161=DIRECTION('center_axis',(1.,1.22464679914735E-16,0.));
#34162=DIRECTION('ref_axis',(-1.22464679914735E-16,1.,0.));
#34163=DIRECTION('center_axis',(1.,1.22464679914735E-16,0.));
#34164=DIRECTION('ref_axis',(-1.22464679914735E-16,1.,0.));
#34165=DIRECTION('',(-1.,-1.22464679914735E-16,0.));
#34166=DIRECTION('center_axis',(1.,1.22464679914735E-16,0.));
#34167=DIRECTION('ref_axis',(-1.22464679914735E-16,1.,0.));
#34168=DIRECTION('center_axis',(1.,1.22464679914735E-16,0.));
#34169=DIRECTION('ref_axis',(-1.22464679914735E-16,1.,0.));
#34170=DIRECTION('',(-0.707106781186546,0.707106781186549,8.65956056235495E-17));
#34171=DIRECTION('center_axis',(1.,1.22464679914735E-16,0.));
#34172=DIRECTION('ref_axis',(-1.22464679914735E-16,1.,0.));
#34173=DIRECTION('center_axis',(-1.,-1.22464679914735E-16,0.));
#34174=DIRECTION('ref_axis',(1.22464679914735E-16,-1.,0.));
#34175=DIRECTION('center_axis',(1.,1.22464679914735E-16,0.));
#34176=DIRECTION('ref_axis',(-1.22464679914735E-16,1.,0.));
#34177=DIRECTION('',(0.707106781186552,-0.707106781186543,8.65956056235488E-17));
#34178=DIRECTION('center_axis',(1.,1.22464679914735E-16,0.));
#34179=DIRECTION('ref_axis',(-1.22464679914735E-16,1.,0.));
#34180=DIRECTION('center_axis',(1.,1.22464679914735E-16,0.));
#34181=DIRECTION('ref_axis',(-1.22464679914735E-16,1.,0.));
#34182=DIRECTION('center_axis',(1.,1.22464679914735E-16,0.));
#34183=DIRECTION('ref_axis',(-1.22464679914735E-16,1.,0.));
#34184=DIRECTION('',(-1.,-1.22464679914735E-16,0.));
#34185=DIRECTION('center_axis',(1.,1.22464679914735E-16,0.));
#34186=DIRECTION('ref_axis',(-1.22464679914735E-16,1.,0.));
#34187=DIRECTION('center_axis',(1.,1.22464679914735E-16,0.));
#34188=DIRECTION('ref_axis',(-1.22464679914735E-16,1.,0.));
#34189=DIRECTION('center_axis',(-1.,-1.22464679914735E-16,0.));
#34190=DIRECTION('ref_axis',(1.22464679914735E-16,-1.,0.));
#34191=DIRECTION('',(0.,0.5,-0.866025403784439));
#34192=DIRECTION('',(0.,1.,0.));
#34193=DIRECTION('',(0.,0.5,0.866025403784439));
#34194=DIRECTION('',(0.,-0.5,0.866025403784438));
#34195=DIRECTION('',(0.,-1.,-1.50231459873716E-16));
#34196=DIRECTION('',(0.,-0.5,-0.866025403784439));
#34197=DIRECTION('center_axis',(1.,1.22464679914735E-16,0.));
#34198=DIRECTION('ref_axis',(-1.22464679914735E-16,1.,0.));
#34199=DIRECTION('center_axis',(-1.06057523872491E-16,0.866025403784439,
0.5));
#34200=DIRECTION('ref_axis',(-5.09861652542584E-33,-0.5,0.866025403784439));
#34201=DIRECTION('',(-1.,-1.22464679914735E-16,0.));
#34202=DIRECTION('',(0.,0.5,-0.866025403784439));
#34203=DIRECTION('',(-1.,-1.22464679914735E-16,0.));
#34204=DIRECTION('center_axis',(0.,0.,1.));
#34205=DIRECTION('ref_axis',(1.,0.,0.));
#34206=DIRECTION('',(0.,1.,0.));
#34207=DIRECTION('',(-1.,-1.22464679914735E-16,0.));
#34208=DIRECTION('center_axis',(1.06057523872491E-16,-0.866025403784439,
0.5));
#34209=DIRECTION('ref_axis',(-8.4117933897259E-34,-0.5,-0.866025403784439));
#34210=DIRECTION('',(0.,0.5,0.866025403784439));
#34211=DIRECTION('',(-1.,-1.22464679914735E-16,0.));
#34212=DIRECTION('center_axis',(1.06057523872491E-16,-0.866025403784439,
-0.5));
#34213=DIRECTION('ref_axis',(-5.93979586439842E-33,0.5,-0.866025403784439));
#34214=DIRECTION('',(0.,-0.5,0.866025403784438));
#34215=DIRECTION('',(-1.,-1.22464679914735E-16,0.));
#34216=DIRECTION('center_axis',(-1.8398047646558E-32,1.50231459873716E-16,
-1.));
#34217=DIRECTION('ref_axis',(0.,1.,1.50231459873716E-16));
#34218=DIRECTION('',(0.,-1.,-1.50231459873716E-16));
#34219=DIRECTION('',(-1.,-1.22464679914735E-16,0.));
#34220=DIRECTION('center_axis',(-1.06057523872491E-16,0.866025403784439,
-0.5));
#34221=DIRECTION('ref_axis',(2.96989793219921E-33,0.5,0.866025403784439));
#34222=DIRECTION('',(0.,-0.5,-0.866025403784439));
#34223=DIRECTION('center_axis',(-1.,0.,0.));
#34224=DIRECTION('ref_axis',(0.,0.,1.));
#56616=CARTESIAN_POINT('',(0.,0.,0.));
#56617=CARTESIAN_POINT('Origin',(25.,2.32682891837997E-15,0.));
#56618=CARTESIAN_POINT('',(0.,-5.,-6.12323399573677E-16));
#56619=CARTESIAN_POINT('Origin',(0.,-7.34788079488413E-16,0.));
#56620=CARTESIAN_POINT('',(-5.4,-5.,-6.12323399573677E-16));
#56621=CARTESIAN_POINT('',(25.,-5.,-6.12323399573677E-16));
#56622=CARTESIAN_POINT('Origin',(-5.4,-1.39609735102798E-15,0.));
#56623=CARTESIAN_POINT('Origin',(-5.4,-1.39609735102798E-15,0.));
#56624=CARTESIAN_POINT('',(-6.,-4.4,-5.38844591624836E-16));
#56625=CARTESIAN_POINT('',(-5.4,-5.,-6.12323399573677E-16));
#56626=CARTESIAN_POINT('Origin',(-6.,-1.46957615897682E-15,0.));
#56627=CARTESIAN_POINT('Origin',(25.,2.32682891837997E-15,0.));
#56628=CARTESIAN_POINT('',(24.4585,-3.,3.67394039744206E-16));
#56629=CARTESIAN_POINT('',(24.4585,3.,-3.67394039744206E-16));
#56630=CARTESIAN_POINT('Origin',(24.4585,2.26051429420614E-15,0.));
#56631=CARTESIAN_POINT('',(25.,2.4585,-3.01079415570377E-16));
#56632=CARTESIAN_POINT('',(25.,2.4585,-3.01079415570377E-16));
#56633=CARTESIAN_POINT('Origin',(25.,2.32682891837997E-15,0.));
#56634=CARTESIAN_POINT('Origin',(24.4585,2.26051429420614E-15,0.));
#56635=CARTESIAN_POINT('Origin',(25.,2.32682891837997E-15,0.));
#56636=CARTESIAN_POINT('',(0.,-3.,-3.67394039744206E-16));
#56637=CARTESIAN_POINT('',(25.,-3.,-3.67394039744206E-16));
#56638=CARTESIAN_POINT('Origin',(0.,-7.34788079488413E-16,0.));
#56639=CARTESIAN_POINT('Origin',(25.,2.4585,0.));
#56640=CARTESIAN_POINT('Origin',(-6.,-1.46957615897682E-15,0.));
#56641=CARTESIAN_POINT('',(-6.,1.44337567297406,2.5));
#56642=CARTESIAN_POINT('',(-6.,2.88675134594813,0.));
#56643=CARTESIAN_POINT('',(-6.,1.44337567297406,2.5));
#56644=CARTESIAN_POINT('',(-6.,-1.44337567297407,2.5));
#56645=CARTESIAN_POINT('',(-6.,-1.44337567297407,2.5));
#56646=CARTESIAN_POINT('',(-6.,-2.88675134594813,-7.77133304087269E-16));
#56647=CARTESIAN_POINT('',(-6.,-2.88675134594813,-7.77133304087269E-16));
#56648=CARTESIAN_POINT('',(-6.,-1.44337567297407,-2.5));
#56649=CARTESIAN_POINT('',(-6.,-1.44337567297407,-2.5));
#56650=CARTESIAN_POINT('',(-6.,1.44337567297406,-2.5));
#56651=CARTESIAN_POINT('',(-6.,1.44337567297406,-2.5));
#56652=CARTESIAN_POINT('',(-6.,2.88675134594813,3.50584097974525E-17));
#56653=CARTESIAN_POINT('Origin',(1.22464679914735E-16,3.,0.));
#56654=CARTESIAN_POINT('Origin',(-3.,1.44337567297406,2.5));
#56655=CARTESIAN_POINT('',(-3.,2.88675134594813,3.50584097974525E-17));
#56656=CARTESIAN_POINT('',(-3.,2.88675134594813,3.50584097974525E-17));
#56657=CARTESIAN_POINT('',(-3.,1.44337567297406,2.5));
#56658=CARTESIAN_POINT('',(-3.,1.44337567297406,2.5));
#56659=CARTESIAN_POINT('',(-3.,1.44337567297406,2.5));
#56660=CARTESIAN_POINT('Origin',(-3.,-1.44337567297407,2.5));
#56661=CARTESIAN_POINT('',(-3.,-1.44337567297407,2.5));
#56662=CARTESIAN_POINT('',(-3.,-1.44337567297407,2.5));
#56663=CARTESIAN_POINT('',(-3.,-1.44337567297407,2.5));
#56664=CARTESIAN_POINT('Origin',(-3.,-2.88675134594813,-7.77133304087269E-16));
#56665=CARTESIAN_POINT('',(-3.,-2.88675134594813,-7.77133304087269E-16));
#56666=CARTESIAN_POINT('',(-3.,-2.88675134594813,-7.77133304087269E-16));
#56667=CARTESIAN_POINT('',(-3.,-2.88675134594813,-7.77133304087269E-16));
#56668=CARTESIAN_POINT('Origin',(-3.,-1.44337567297406,-2.5));
#56669=CARTESIAN_POINT('',(-3.,-1.44337567297406,-2.5));
#56670=CARTESIAN_POINT('',(-3.,-1.44337567297406,-2.5));
#56671=CARTESIAN_POINT('',(-3.,-1.44337567297406,-2.5));
#56672=CARTESIAN_POINT('Origin',(-3.,1.44337567297407,-2.5));
#56673=CARTESIAN_POINT('',(-3.,1.44337567297407,-2.5));
#56674=CARTESIAN_POINT('',(-3.,1.44337567297407,-2.5));
#56675=CARTESIAN_POINT('',(-3.,1.44337567297407,-2.5));
#56676=CARTESIAN_POINT('Origin',(-3.,2.88675134594813,3.50584097974525E-17));
#56677=CARTESIAN_POINT('',(-3.,2.88675134594813,3.50584097974525E-17));
#56678=CARTESIAN_POINT('Origin',(-3.,3.67394039744206E-16,0.));
#57036=UNCERTAINTY_MEASURE_WITH_UNIT(LENGTH_MEASURE(0.01),#57080,
'DISTANCE_ACCURACY_VALUE',
'Maximum model space distance between geometric entities at asserted c
onnectivities');
#57040=UNCERTAINTY_MEASURE_WITH_UNIT(LENGTH_MEASURE(0.01),#57080,
'DISTANCE_ACCURACY_VALUE',
'Maximum model space distance between geometric entities at asserted c
onnectivities');
#57075=(
GEOMETRIC_REPRESENTATION_CONTEXT(3)
GLOBAL_UNCERTAINTY_ASSIGNED_CONTEXT((#57036))
GLOBAL_UNIT_ASSIGNED_CONTEXT((#57080,#57082,#57083))
REPRESENTATION_CONTEXT('','3D')
);
#57079=(
GEOMETRIC_REPRESENTATION_CONTEXT(3)
GLOBAL_UNCERTAINTY_ASSIGNED_CONTEXT((#57040))
GLOBAL_UNIT_ASSIGNED_CONTEXT((#57080,#57082,#57083))
REPRESENTATION_CONTEXT('','3D')
);
#57080=(
LENGTH_UNIT()
NAMED_UNIT(*)
SI_UNIT(.MILLI.,.METRE.)
);
#57082=(
NAMED_UNIT(*)
PLANE_ANGLE_UNIT()
SI_UNIT($,.RADIAN.)
);
#57083=(
NAMED_UNIT(*)
SI_UNIT($,.STERADIAN.)
SOLID_ANGLE_UNIT()
);
#57118=SHAPE_DEFINITION_REPRESENTATION(#57182,#57283);
#57182=PRODUCT_DEFINITION_SHAPE('',$,#57322);
#57283=SHAPE_REPRESENTATION('',(#27293),#57075);
#57287=PRODUCT_DEFINITION_CONTEXT('part definition',#57403,'design');
#57322=PRODUCT_DEFINITION('Socket head cap screw M6x25',
'Socket Head Cap Screw M6x25',#57360,#57287);
#57360=PRODUCT_DEFINITION_FORMATION('',$,#57439);
#57403=APPLICATION_CONTEXT(
'Core Data for Automotive Mechanical Design Process');
#57404=PRODUCT_CONTEXT('part definition',#57403,'mechanical');
#57439=PRODUCT('Socket head cap screw M6x25',
'Socket Head Cap Screw M6x25',$,(#57404));
#57444=PRESENTATION_STYLE_ASSIGNMENT((#57446));
#57446=SURFACE_STYLE_USAGE(.BOTH.,#57448);
#57448=SURFACE_SIDE_STYLE('',(#57450));
#57450=SURFACE_STYLE_FILL_AREA(#57452);
#57452=FILL_AREA_STYLE('Opaque(202,209,238)',(#57454));
#57454=FILL_AREA_STYLE_COLOUR('Opaque(202,209,238)',#57456);
#57456=COLOUR_RGB('Opaque(202,209,238)',0.792156862745098,0.819607843137255,
0.933333333333333);
ENDSEC;
END-ISO-10303-21;
